ISO-10303-21;
HEADER;
/* Generated by software containing ST-Developer
 * from STEP Tools, Inc. (www.steptools.com) 
 */

FILE_DESCRIPTION(
/* description */ ('Rigid flange shaft coupling assembly'),
/* implementation_level */ '2;1');

FILE_NAME(
/* name */ 'Flat Washer - M6.step',
/* time_stamp */ '2026-10-27T10:47:16-07:00',
/* author */ (''),
/* organization */ (''),
/* preprocessor_version */ 'ST-DEVELOPER v20.2',
/* originating_system */ 'Autodesk Translation Framework v15.17.0.0',
/* authorisation */ '');

FILE_SCHEMA (('AUTOMOTIVE_DESIGN { 1 0 10303 214 3 1 1 }'));
ENDSEC;

DATA;
#10=MECHANICAL_DESIGN_GEOMETRIC_PRESENTATION_REPRESENTATION('',(#424),#9141);
#367=SHAPE_REPRESENTATION_RELATIONSHIP('SRR','None',#9303,#395);
#395=ADVANCED_BREP_SHAPE_REPRESENTATION('',(#450),#9138);
#424=STYLED_ITEM('',(#9507),#450);
#450=MANIFOLD_SOLID_BREP('Body1',#4781);
#565=FACE_BOUND('',#1376,.T.);
#566=FACE_BOUND('',#1378,.T.);
#725=PLANE('',#5545);
#726=PLANE('',#5546);
#989=FACE_OUTER_BOUND('',#1373,.T.);
#990=FACE_OUTER_BOUND('',#1374,.T.);
#991=FACE_OUTER_BOUND('',#1375,.T.);
#992=FACE_OUTER_BOUND('',#1377,.T.);
#1373=EDGE_LOOP('',(#4287,#4288,#4289,#4290));
#1374=EDGE_LOOP('',(#4291,#4292,#4293,#4294));
#1375=EDGE_LOOP('',(#4295));
#1376=EDGE_LOOP('',(#4296));
#1377=EDGE_LOOP('',(#4297));
#1378=EDGE_LOOP('',(#4298));
#1718=LINE('',#8873,#2063);
#1719=LINE('',#8879,#2064);
#2063=VECTOR('',#6851,0.32);
#2064=VECTOR('',#6858,0.6);
#2264=CIRCLE('',#5540,0.32);
#2265=CIRCLE('',#5541,0.32);
#2266=CIRCLE('',#5543,0.6);
#2267=CIRCLE('',#5544,0.6);
#2629=VERTEX_POINT('',#8870);
#2630=VERTEX_POINT('',#8872);
#2631=VERTEX_POINT('',#8876);
#2632=VERTEX_POINT('',#8878);
#3187=EDGE_CURVE('',#2629,#2629,#2264,.T.);
#3188=EDGE_CURVE('',#2629,#2630,#1718,.T.);
#3189=EDGE_CURVE('',#2630,#2630,#2265,.T.);
#3190=EDGE_CURVE('',#2631,#2631,#2266,.T.);
#3191=EDGE_CURVE('',#2631,#2632,#1719,.T.);
#3192=EDGE_CURVE('',#2632,#2632,#2267,.T.);
#4287=ORIENTED_EDGE('',*,*,#3187,.F.);
#4288=ORIENTED_EDGE('',*,*,#3188,.T.);
#4289=ORIENTED_EDGE('',*,*,#3189,.T.);
#4290=ORIENTED_EDGE('',*,*,#3188,.F.);
#4291=ORIENTED_EDGE('',*,*,#3190,.F.);
#4292=ORIENTED_EDGE('',*,*,#3191,.T.);
#4293=ORIENTED_EDGE('',*,*,#3192,.T.);
#4294=ORIENTED_EDGE('',*,*,#3191,.F.);
#4295=ORIENTED_EDGE('',*,*,#3190,.T.);
#4296=ORIENTED_EDGE('',*,*,#3187,.T.);
#4297=ORIENTED_EDGE('',*,*,#3192,.F.);
#4298=ORIENTED_EDGE('',*,*,#3189,.F.);
#4476=CYLINDRICAL_SURFACE('',#5539,0.32);
#4477=CYLINDRICAL_SURFACE('',#5542,0.6);
#4725=ADVANCED_FACE('',(#989),#4476,.F.);
#4726=ADVANCED_FACE('',(#990),#4477,.T.);
#4727=ADVANCED_FACE('',(#991,#565),#725,.T.);
#4728=ADVANCED_FACE('',(#992,#566),#726,.F.);
#4781=CLOSED_SHELL('',(#4725,#4726,#4727,#4728));
#5538=AXIS2_PLACEMENT_3D('',#8868,#6845,#6846);
#5539=AXIS2_PLACEMENT_3D('',#8869,#6847,#6848);
#5540=AXIS2_PLACEMENT_3D('',#8871,#6849,#6850);
#5541=AXIS2_PLACEMENT_3D('',#8874,#6852,#6853);
#5542=AXIS2_PLACEMENT_3D('',#8875,#6854,#6855);
#5543=AXIS2_PLACEMENT_3D('',#8877,#6856,#6857);
#5544=AXIS2_PLACEMENT_3D('',#8880,#6859,#6860);
#5545=AXIS2_PLACEMENT_3D('',#8881,#6861,#6862);
#5546=AXIS2_PLACEMENT_3D('',#8882,#6863,#6864);
#6845=DIRECTION('axis',(0.,0.,1.));
#6846=DIRECTION('refdir',(1.,0.,0.));
#6847=DIRECTION('center_axis',(0.,1.,0.));
#6848=DIRECTION('ref_axis',(1.,0.,0.));
#6849=DIRECTION('center_axis',(0.,-1.,0.));
#6850=DIRECTION('ref_axis',(1.,0.,0.));
#6851=DIRECTION('',(0.,-1.,0.));
#6852=DIRECTION('center_axis',(0.,-1.,0.));
#6853=DIRECTION('ref_axis',(1.,0.,0.));
#6854=DIRECTION('center_axis',(0.,1.,0.));
#6855=DIRECTION('ref_axis',(1.,0.,0.));
#6856=DIRECTION('center_axis',(0.,1.,0.));
#6857=DIRECTION('ref_axis',(1.,0.,0.));
#6858=DIRECTION('',(0.,-1.,0.));
#6859=DIRECTION('center_axis',(0.,1.,0.));
#6860=DIRECTION('ref_axis',(1.,0.,0.));
#6861=DIRECTION('center_axis',(0.,1.,0.));
#6862=DIRECTION('ref_axis',(1.,0.,0.));
#6863=DIRECTION('center_axis',(0.,1.,0.));
#6864=DIRECTION('ref_axis',(1.,0.,0.));
#8868=CARTESIAN_POINT('',(0.,0.,0.));
#8869=CARTESIAN_POINT('Origin',(0.,0.,0.));
#8870=CARTESIAN_POINT('',(-0.32,0.16,3.91886975727153E-17));
#8871=CARTESIAN_POINT('Origin',(0.,0.16,0.));
#8872=CARTESIAN_POINT('',(-0.32,0.,3.91886975727153E-17));
#8873=CARTESIAN_POINT('',(-0.32,0.,3.91886975727153E-17));
#8874=CARTESIAN_POINT('Origin',(0.,0.,0.));
#8875=CARTESIAN_POINT('Origin',(0.,0.,0.));
#8876=CARTESIAN_POINT('',(-0.6,0.16,7.34788079488412E-17));
#8877=CARTESIAN_POINT('Origin',(0.,0.16,0.));
#8878=CARTESIAN_POINT('',(-0.6,0.,7.34788079488412E-17));
#8879=CARTESIAN_POINT('',(-0.6,0.,7.34788079488412E-17));
#8880=CARTESIAN_POINT('Origin',(0.,0.,0.));
#8881=CARTESIAN_POINT('Origin',(0.,0.16,0.));
#8882=CARTESIAN_POINT('Origin',(0.,0.,0.));
#9105=UNCERTAINTY_MEASURE_WITH_UNIT(LENGTH_MEASURE(0.001),#9142,
'DISTANCE_ACCURACY_VALUE',
'Maximum model space distance between geometric entities at asserted c
onnectivities');
#9108=UNCERTAINTY_MEASURE_WITH_UNIT(LENGTH_MEASURE(0.001),#9142,
'DISTANCE_ACCURACY_VALUE',
'Maximum model space distance between geometric entities at asserted c
onnectivities');
#9138=(
GEOMETRIC_REPRESENTATION_CONTEXT(3)
GLOBAL_UNCERTAINTY_ASSIGNED_CONTEXT((#9105))
GLOBAL_UNIT_ASSIGNED_CONTEXT((#9142,#9144,#9145))
REPRESENTATION_CONTEXT('','3D')
);
#9141=(
GEOMETRIC_REPRESENTATION_CONTEXT(3)
GLOBAL_UNCERTAINTY_ASSIGNED_CONTEXT((#9108))
GLOBAL_UNIT_ASSIGNED_CONTEXT((#9142,#9144,#9145))
REPRESENTATION_CONTEXT('','3D')
);
#9142=(
LENGTH_UNIT()
NAMED_UNIT(*)
SI_UNIT(.CENTI.,.METRE.)
);
#9144=(
NAMED_UNIT(*)
PLANE_ANGLE_UNIT()
SI_UNIT($,.RADIAN.)
);
#9145=(
NAMED_UNIT(*)
SI_UNIT($,.STERADIAN.)
SOLID_ANGLE_UNIT()
);
#9175=SHAPE_DEFINITION_REPRESENTATION(#9209,#9303);
#9209=PRODUCT_DEFINITION_SHAPE('',$,#9336);
#9303=SHAPE_REPRESENTATION('',(#5538),#9138);
#9306=PRODUCT_DEFINITION_CONTEXT('part definition',#9404,'design');
#9336=PRODUCT_DEFINITION('Flat Washer - M6','Flat Washer - M6',#9368,#9306);
#9368=PRODUCT_DEFINITION_FORMATION('',$,#9435);
#9404=APPLICATION_CONTEXT(
'Core Data for Automotive Mechanical Design Process');
#9405=PRODUCT_CONTEXT('part definition',#9404,'mechanical');
#9435=PRODUCT('Flat Washer - M6','Flat Washer - M6','Flat Washer - M6',
(#9405));
#9501=COLOUR_RGB('Black',0.12,0.14,0.17);
#9502=FILL_AREA_STYLE_COLOUR('',#9501);
#9503=FILL_AREA_STYLE('',(#9502));
#9504=SURFACE_STYLE_FILL_AREA(#9503);
#9505=SURFACE_SIDE_STYLE('',(#9504));
#9506=SURFACE_STYLE_USAGE(.BOTH.,#9505);
#9507=PRESENTATION_STYLE_ASSIGNMENT((#9506));
ENDSEC;
END-ISO-10303-21;
